ISO-10303-21;
HEADER;
/* Generated by software containing ST-Developer
 * from STEP Tools, Inc. (www.steptools.com) 
 */

FILE_DESCRIPTION(
/* description */ ('Five-roller gravity conveyor'),
/* implementation_level */ '2;1');

FILE_NAME(
/* name */ 'Axle.step',
/* time_stamp */ '2026-10-29T15:36:43-07:00',
/* author */ (''),
/* organization */ (''),
/* preprocessor_version */ 'ST-DEVELOPER v20.2',
/* originating_system */ 'Autodesk Translation Framework v15.17.0.0',
/* authorisation */ '');

FILE_SCHEMA (('AUTOMOTIVE_DESIGN { 1 0 10303 214 3 1 1 }'));
ENDSEC;

DATA;
#10=MECHANICAL_DESIGN_GEOMETRIC_PRESENTATION_REPRESENTATION('',(#313),#7806);
#277=SHAPE_REPRESENTATION_RELATIONSHIP('SRR','None',#7914,#295);
#295=ADVANCED_BREP_SHAPE_REPRESENTATION('',(#339),#7787);
#313=STYLED_ITEM('',(#8091),#339);
#339=MANIFOLD_SOLID_BREP('Body1',#4200);
#364=FACE_BOUND('',#938,.T.);
#365=FACE_BOUND('',#940,.T.);
#366=FACE_BOUND('',#945,.T.);
#367=FACE_BOUND('',#947,.T.);
#423=CIRCLE('',#4481,0.165);
#424=CIRCLE('',#4482,0.165);
#425=CIRCLE('',#4485,0.165);
#426=CIRCLE('',#4486,0.165);
#427=CIRCLE('',#4489,0.6);
#428=CIRCLE('',#4490,0.5);
#429=CIRCLE('',#4492,0.6);
#430=CIRCLE('',#4493,0.5);
#431=CIRCLE('',#4496,0.5);
#432=CIRCLE('',#4498,0.5);
#595=CYLINDRICAL_SURFACE('',#4480,0.165);
#596=CYLINDRICAL_SURFACE('',#4484,0.165);
#597=CYLINDRICAL_SURFACE('',#4494,0.6);
#598=CYLINDRICAL_SURFACE('',#4495,0.5);
#599=CYLINDRICAL_SURFACE('',#4497,0.5);
#699=FACE_OUTER_BOUND('',#933,.T.);
#700=FACE_OUTER_BOUND('',#934,.T.);
#701=FACE_OUTER_BOUND('',#935,.T.);
#702=FACE_OUTER_BOUND('',#936,.T.);
#703=FACE_OUTER_BOUND('',#937,.T.);
#704=FACE_OUTER_BOUND('',#939,.T.);
#705=FACE_OUTER_BOUND('',#941,.T.);
#706=FACE_OUTER_BOUND('',#942,.T.);
#707=FACE_OUTER_BOUND('',#943,.T.);
#708=FACE_OUTER_BOUND('',#944,.T.);
#709=FACE_OUTER_BOUND('',#946,.T.);
#933=EDGE_LOOP('',(#3024,#3025,#3026,#3027));
#934=EDGE_LOOP('',(#3028));
#935=EDGE_LOOP('',(#3029,#3030,#3031,#3032));
#936=EDGE_LOOP('',(#3033));
#937=EDGE_LOOP('',(#3034));
#938=EDGE_LOOP('',(#3035));
#939=EDGE_LOOP('',(#3036));
#940=EDGE_LOOP('',(#3037));
#941=EDGE_LOOP('',(#3038,#3039,#3040,#3041));
#942=EDGE_LOOP('',(#3042,#3043,#3044,#3045));
#943=EDGE_LOOP('',(#3046,#3047,#3048,#3049));
#944=EDGE_LOOP('',(#3050));
#945=EDGE_LOOP('',(#3051));
#946=EDGE_LOOP('',(#3052));
#947=EDGE_LOOP('',(#3053));
#1308=LINE('',#6497,#1649);
#1309=LINE('',#6504,#1650);
#1310=LINE('',#6518,#1651);
#1311=LINE('',#6521,#1652);
#1312=LINE('',#6526,#1653);
#1649=VECTOR('',#5154,0.165);
#1650=VECTOR('',#5163,0.165);
#1651=VECTOR('',#5182,0.6);
#1652=VECTOR('',#5185,0.5);
#1653=VECTOR('',#5192,0.5);
#1947=VERTEX_POINT('',#6494);
#1948=VERTEX_POINT('',#6496);
#1949=VERTEX_POINT('',#6501);
#1950=VERTEX_POINT('',#6503);
#1951=VERTEX_POINT('',#6508);
#1952=VERTEX_POINT('',#6510);
#1953=VERTEX_POINT('',#6513);
#1954=VERTEX_POINT('',#6515);
#1955=VERTEX_POINT('',#6520);
#1956=VERTEX_POINT('',#6524);
#2355=EDGE_CURVE('',#1947,#1947,#423,.T.);
#2356=EDGE_CURVE('',#1947,#1948,#1308,.T.);
#2357=EDGE_CURVE('',#1948,#1948,#424,.T.);
#2358=EDGE_CURVE('',#1949,#1949,#425,.T.);
#2359=EDGE_CURVE('',#1949,#1950,#1309,.T.);
#2360=EDGE_CURVE('',#1950,#1950,#426,.T.);
#2361=EDGE_CURVE('',#1951,#1951,#427,.T.);
#2362=EDGE_CURVE('',#1952,#1952,#428,.T.);
#2363=EDGE_CURVE('',#1953,#1953,#429,.T.);
#2364=EDGE_CURVE('',#1954,#1954,#430,.T.);
#2365=EDGE_CURVE('',#1951,#1953,#1310,.T.);
#2366=EDGE_CURVE('',#1954,#1955,#1311,.T.);
#2367=EDGE_CURVE('',#1955,#1955,#431,.T.);
#2368=EDGE_CURVE('',#1956,#1956,#432,.T.);
#2369=EDGE_CURVE('',#1956,#1952,#1312,.T.);
#3024=ORIENTED_EDGE('',*,*,#2355,.F.);
#3025=ORIENTED_EDGE('',*,*,#2356,.T.);
#3026=ORIENTED_EDGE('',*,*,#2357,.F.);
#3027=ORIENTED_EDGE('',*,*,#2356,.F.);
#3028=ORIENTED_EDGE('',*,*,#2355,.T.);
#3029=ORIENTED_EDGE('',*,*,#2358,.F.);
#3030=ORIENTED_EDGE('',*,*,#2359,.T.);
#3031=ORIENTED_EDGE('',*,*,#2360,.T.);
#3032=ORIENTED_EDGE('',*,*,#2359,.F.);
#3033=ORIENTED_EDGE('',*,*,#2360,.F.);
#3034=ORIENTED_EDGE('',*,*,#2361,.T.);
#3035=ORIENTED_EDGE('',*,*,#2362,.F.);
#3036=ORIENTED_EDGE('',*,*,#2363,.F.);
#3037=ORIENTED_EDGE('',*,*,#2364,.F.);
#3038=ORIENTED_EDGE('',*,*,#2361,.F.);
#3039=ORIENTED_EDGE('',*,*,#2365,.T.);
#3040=ORIENTED_EDGE('',*,*,#2363,.T.);
#3041=ORIENTED_EDGE('',*,*,#2365,.F.);
#3042=ORIENTED_EDGE('',*,*,#2364,.T.);
#3043=ORIENTED_EDGE('',*,*,#2366,.T.);
#3044=ORIENTED_EDGE('',*,*,#2367,.T.);
#3045=ORIENTED_EDGE('',*,*,#2366,.F.);
#3046=ORIENTED_EDGE('',*,*,#2368,.F.);
#3047=ORIENTED_EDGE('',*,*,#2369,.T.);
#3048=ORIENTED_EDGE('',*,*,#2362,.T.);
#3049=ORIENTED_EDGE('',*,*,#2369,.F.);
#3050=ORIENTED_EDGE('',*,*,#2368,.T.);
#3051=ORIENTED_EDGE('',*,*,#2357,.T.);
#3052=ORIENTED_EDGE('',*,*,#2367,.F.);
#3053=ORIENTED_EDGE('',*,*,#2358,.T.);
#3868=PLANE('',#4483);
#3869=PLANE('',#4487);
#3870=PLANE('',#4488);
#3871=PLANE('',#4491);
#3872=PLANE('',#4499);
#3873=PLANE('',#4500);
#4014=ADVANCED_FACE('',(#699),#595,.F.);
#4015=ADVANCED_FACE('',(#700),#3868,.T.);
#4016=ADVANCED_FACE('',(#701),#596,.F.);
#4017=ADVANCED_FACE('',(#702),#3869,.F.);
#4018=ADVANCED_FACE('',(#703,#364),#3870,.T.);
#4019=ADVANCED_FACE('',(#704,#365),#3871,.F.);
#4020=ADVANCED_FACE('',(#705),#597,.T.);
#4021=ADVANCED_FACE('',(#706),#598,.T.);
#4022=ADVANCED_FACE('',(#707),#599,.T.);
#4023=ADVANCED_FACE('',(#708,#366),#3872,.T.);
#4024=ADVANCED_FACE('',(#709,#367),#3873,.F.);
#4200=CLOSED_SHELL('',(#4014,#4015,#4016,#4017,#4018,#4019,#4020,#4021,
#4022,#4023,#4024));
#4479=AXIS2_PLACEMENT_3D('',#6492,#5148,#5149);
#4480=AXIS2_PLACEMENT_3D('',#6493,#5150,#5151);
#4481=AXIS2_PLACEMENT_3D('',#6495,#5152,#5153);
#4482=AXIS2_PLACEMENT_3D('',#6498,#5155,#5156);
#4483=AXIS2_PLACEMENT_3D('',#6499,#5157,#5158);
#4484=AXIS2_PLACEMENT_3D('',#6500,#5159,#5160);
#4485=AXIS2_PLACEMENT_3D('',#6502,#5161,#5162);
#4486=AXIS2_PLACEMENT_3D('',#6505,#5164,#5165);
#4487=AXIS2_PLACEMENT_3D('',#6506,#5166,#5167);
#4488=AXIS2_PLACEMENT_3D('',#6507,#5168,#5169);
#4489=AXIS2_PLACEMENT_3D('',#6509,#5170,#5171);
#4490=AXIS2_PLACEMENT_3D('',#6511,#5172,#5173);
#4491=AXIS2_PLACEMENT_3D('',#6512,#5174,#5175);
#4492=AXIS2_PLACEMENT_3D('',#6514,#5176,#5177);
#4493=AXIS2_PLACEMENT_3D('',#6516,#5178,#5179);
#4494=AXIS2_PLACEMENT_3D('',#6517,#5180,#5181);
#4495=AXIS2_PLACEMENT_3D('',#6519,#5183,#5184);
#4496=AXIS2_PLACEMENT_3D('',#6522,#5186,#5187);
#4497=AXIS2_PLACEMENT_3D('',#6523,#5188,#5189);
#4498=AXIS2_PLACEMENT_3D('',#6525,#5190,#5191);
#4499=AXIS2_PLACEMENT_3D('',#6527,#5193,#5194);
#4500=AXIS2_PLACEMENT_3D('',#6528,#5195,#5196);
#5148=DIRECTION('axis',(0.,0.,1.));
#5149=DIRECTION('refdir',(1.,0.,0.));
#5150=DIRECTION('center_axis',(0.,1.,0.));
#5151=DIRECTION('ref_axis',(1.,0.,0.));
#5152=DIRECTION('center_axis',(0.,1.,0.));
#5153=DIRECTION('ref_axis',(1.,0.,0.));
#5154=DIRECTION('',(0.,1.,0.));
#5155=DIRECTION('center_axis',(0.,-1.,0.));
#5156=DIRECTION('ref_axis',(1.,0.,0.));
#5157=DIRECTION('center_axis',(0.,1.,0.));
#5158=DIRECTION('ref_axis',(1.,0.,0.));
#5159=DIRECTION('center_axis',(0.,1.,0.));
#5160=DIRECTION('ref_axis',(1.,0.,0.));
#5161=DIRECTION('center_axis',(0.,1.,0.));
#5162=DIRECTION('ref_axis',(1.,0.,0.));
#5163=DIRECTION('',(0.,1.,0.));
#5164=DIRECTION('center_axis',(0.,1.,0.));
#5165=DIRECTION('ref_axis',(1.,0.,0.));
#5166=DIRECTION('center_axis',(0.,1.,0.));
#5167=DIRECTION('ref_axis',(1.,0.,0.));
#5168=DIRECTION('center_axis',(0.,1.,0.));
#5169=DIRECTION('ref_axis',(1.,0.,0.));
#5170=DIRECTION('center_axis',(0.,1.,0.));
#5171=DIRECTION('ref_axis',(1.,0.,0.));
#5172=DIRECTION('center_axis',(0.,1.,0.));
#5173=DIRECTION('ref_axis',(1.,0.,0.));
#5174=DIRECTION('center_axis',(0.,1.,0.));
#5175=DIRECTION('ref_axis',(1.,0.,0.));
#5176=DIRECTION('center_axis',(0.,1.,0.));
#5177=DIRECTION('ref_axis',(1.,0.,0.));
#5178=DIRECTION('center_axis',(0.,-1.,0.));
#5179=DIRECTION('ref_axis',(1.,0.,0.));
#5180=DIRECTION('center_axis',(0.,1.,0.));
#5181=DIRECTION('ref_axis',(1.,0.,0.));
#5182=DIRECTION('',(0.,-1.,0.));
#5183=DIRECTION('center_axis',(0.,1.,0.));
#5184=DIRECTION('ref_axis',(1.,0.,0.));
#5185=DIRECTION('',(0.,-1.,0.));
#5186=DIRECTION('center_axis',(0.,1.,0.));
#5187=DIRECTION('ref_axis',(1.,0.,0.));
#5188=DIRECTION('center_axis',(0.,1.,0.));
#5189=DIRECTION('ref_axis',(1.,0.,0.));
#5190=DIRECTION('center_axis',(0.,1.,0.));
#5191=DIRECTION('ref_axis',(1.,0.,0.));
#5192=DIRECTION('',(0.,-1.,0.));
#5193=DIRECTION('center_axis',(0.,1.,0.));
#5194=DIRECTION('ref_axis',(1.,0.,0.));
#5195=DIRECTION('center_axis',(0.,1.,0.));
#5196=DIRECTION('ref_axis',(1.,0.,0.));
#6492=CARTESIAN_POINT('',(0.,0.,0.));
#6493=CARTESIAN_POINT('Origin',(0.,30.8,4.5));
#6494=CARTESIAN_POINT('',(-0.165,30.8,4.5));
#6495=CARTESIAN_POINT('Origin',(0.,30.8,4.5));
#6496=CARTESIAN_POINT('',(-0.165,32.5,4.5));
#6497=CARTESIAN_POINT('',(-0.165,30.8,4.5));
#6498=CARTESIAN_POINT('Origin',(0.,32.5,4.5));
#6499=CARTESIAN_POINT('Origin',(0.,30.8,4.5));
#6500=CARTESIAN_POINT('Origin',(0.,-2.6,4.5));
#6501=CARTESIAN_POINT('',(-0.165,-2.5,4.5));
#6502=CARTESIAN_POINT('Origin',(0.,-2.5,4.5));
#6503=CARTESIAN_POINT('',(-0.165,-0.8,4.5));
#6504=CARTESIAN_POINT('',(-0.165,-2.6,4.5));
#6505=CARTESIAN_POINT('Origin',(0.,-0.8,4.5));
#6506=CARTESIAN_POINT('Origin',(0.,-0.8,4.5));
#6507=CARTESIAN_POINT('Origin',(0.,29.1,4.5));
#6508=CARTESIAN_POINT('',(-0.6,29.1,4.5));
#6509=CARTESIAN_POINT('Origin',(0.,29.1,4.5));
#6510=CARTESIAN_POINT('',(-0.5,29.1,4.5));
#6511=CARTESIAN_POINT('Origin',(0.,29.1,4.5));
#6512=CARTESIAN_POINT('Origin',(0.,0.9,4.5));
#6513=CARTESIAN_POINT('',(-0.6,0.9,4.5));
#6514=CARTESIAN_POINT('Origin',(0.,0.9,4.5));
#6515=CARTESIAN_POINT('',(-0.5,0.9,4.5));
#6516=CARTESIAN_POINT('Origin',(0.,0.9,4.5));
#6517=CARTESIAN_POINT('Origin',(0.,0.9,4.5));
#6518=CARTESIAN_POINT('',(-0.6,0.9,4.5));
#6519=CARTESIAN_POINT('Origin',(0.,-2.5,4.5));
#6520=CARTESIAN_POINT('',(-0.5,-2.5,4.5));
#6521=CARTESIAN_POINT('',(-0.5,-2.5,4.5));
#6522=CARTESIAN_POINT('Origin',(0.,-2.5,4.5));
#6523=CARTESIAN_POINT('Origin',(0.,-2.5,4.5));
#6524=CARTESIAN_POINT('',(-0.5,32.5,4.5));
#6525=CARTESIAN_POINT('Origin',(0.,32.5,4.5));
#6526=CARTESIAN_POINT('',(-0.5,-2.5,4.5));
#6527=CARTESIAN_POINT('Origin',(0.,32.5,4.5));
#6528=CARTESIAN_POINT('Origin',(0.,-2.5,4.5));
#7763=UNCERTAINTY_MEASURE_WITH_UNIT(LENGTH_MEASURE(0.001),#7807,
'DISTANCE_ACCURACY_VALUE',
'Maximum model space distance between geometric entities at asserted c
onnectivities');
#7782=UNCERTAINTY_MEASURE_WITH_UNIT(LENGTH_MEASURE(0.001),#7807,
'DISTANCE_ACCURACY_VALUE',
'Maximum model space distance between geometric entities at asserted c
onnectivities');
#7787=(
GEOMETRIC_REPRESENTATION_CONTEXT(3)
GLOBAL_UNCERTAINTY_ASSIGNED_CONTEXT((#7763))
GLOBAL_UNIT_ASSIGNED_CONTEXT((#7807,#7809,#7810))
REPRESENTATION_CONTEXT('','3D')
);
#7806=(
GEOMETRIC_REPRESENTATION_CONTEXT(3)
GLOBAL_UNCERTAINTY_ASSIGNED_CONTEXT((#7782))
GLOBAL_UNIT_ASSIGNED_CONTEXT((#7807,#7809,#7810))
REPRESENTATION_CONTEXT('','3D')
);
#7807=(
LENGTH_UNIT()
NAMED_UNIT(*)
SI_UNIT(.CENTI.,.METRE.)
);
#7809=(
NAMED_UNIT(*)
PLANE_ANGLE_UNIT()
SI_UNIT($,.RADIAN.)
);
#7810=(
NAMED_UNIT(*)
SI_UNIT($,.STERADIAN.)
SOLID_ANGLE_UNIT()
);
#7815=SHAPE_DEFINITION_REPRESENTATION(#7838,#7914);
#7838=PRODUCT_DEFINITION_SHAPE('',$,#7938);
#7914=SHAPE_REPRESENTATION('',(#4479),#7787);
#7933=PRODUCT_DEFINITION_CONTEXT('part definition',#8004,'design');
#7938=PRODUCT_DEFINITION('Axle','Axle',#7961,#7933);
#7961=PRODUCT_DEFINITION_FORMATION('',$,#8010);
#8004=APPLICATION_CONTEXT(
'Core Data for Automotive Mechanical Design Process');
#8005=PRODUCT_CONTEXT('part definition',#8004,'mechanical');
#8010=PRODUCT('Axle','Axle','Axle',(#8005));
#8085=COLOUR_RGB('Grey',0.48,0.52,0.57);
#8086=FILL_AREA_STYLE_COLOUR('',#8085);
#8087=FILL_AREA_STYLE('',(#8086));
#8088=SURFACE_STYLE_FILL_AREA(#8087);
#8089=SURFACE_SIDE_STYLE('',(#8088));
#8090=SURFACE_STYLE_USAGE(.BOTH.,#8089);
#8091=PRESENTATION_STYLE_ASSIGNMENT((#8090));
ENDSEC;
END-ISO-10303-21;
